ISO-10303-21;
HEADER;
/* Generated by software containing ST-Developer
 * from STEP Tools, Inc. (www.steptools.com) 
 */

FILE_DESCRIPTION(
/* description */ (''),
/* implementation_level */ '2;1');

FILE_NAME(
/* name */ 'Screw_02.step',
/* time_stamp */ '2026-10-05T19:45:59-07:00',
/* author */ (''),
/* organization */ (''),
/* preprocessor_version */ 'ST-DEVELOPER v20.2',
/* originating_system */ 'Autodesk Translation Framework v15.15.0.0',
/* authorisation */ '');

FILE_SCHEMA (('AUTOMOTIVE_DESIGN { 1 0 10303 214 3 1 1 }'));
ENDSEC;

DATA;
#10=MECHANICAL_DESIGN_GEOMETRIC_PRESENTATION_REPRESENTATION('',(#98),#2462);
#51=TOROIDAL_SURFACE('',#1547,13.,2.);
#70=FACE_BOUND('',#323,.T.);
#71=FACE_BOUND('',#339,.T.);
#80=SHAPE_REPRESENTATION_RELATIONSHIP('SRR','None',#2506,#89);
#89=ADVANCED_BREP_SHAPE_REPRESENTATION('',(#107),#2461);
#98=STYLED_ITEM('',(#2552),#107);
#107=MANIFOLD_SOLID_BREP('Body1',#1335);
#150=PLANE('',#1545);
#151=PLANE('',#1551);
#152=PLANE('',#1554);
#153=PLANE('',#1555);
#154=PLANE('',#1556);
#155=PLANE('',#1557);
#156=PLANE('',#1558);
#157=PLANE('',#1559);
#158=PLANE('',#1560);
#159=PLANE('',#1561);
#160=PLANE('',#1562);
#161=PLANE('',#1563);
#162=PLANE('',#1564);
#163=PLANE('',#1565);
#164=PLANE('',#1568);
#227=FACE_OUTER_BOUND('',#320,.T.);
#228=FACE_OUTER_BOUND('',#321,.T.);
#229=FACE_OUTER_BOUND('',#322,.T.);
#230=FACE_OUTER_BOUND('',#324,.T.);
#231=FACE_OUTER_BOUND('',#325,.T.);
#232=FACE_OUTER_BOUND('',#326,.T.);
#233=FACE_OUTER_BOUND('',#327,.T.);
#234=FACE_OUTER_BOUND('',#328,.T.);
#235=FACE_OUTER_BOUND('',#329,.T.);
#236=FACE_OUTER_BOUND('',#330,.T.);
#237=FACE_OUTER_BOUND('',#331,.T.);
#238=FACE_OUTER_BOUND('',#332,.T.);
#239=FACE_OUTER_BOUND('',#333,.T.);
#240=FACE_OUTER_BOUND('',#334,.T.);
#241=FACE_OUTER_BOUND('',#335,.T.);
#242=FACE_OUTER_BOUND('',#336,.T.);
#243=FACE_OUTER_BOUND('',#337,.T.);
#244=FACE_OUTER_BOUND('',#338,.T.);
#320=EDGE_LOOP('',(#1162));
#321=EDGE_LOOP('',(#1163,#1164,#1165,#1166));
#322=EDGE_LOOP('',(#1167));
#323=EDGE_LOOP('',(#1168,#1169,#1170,#1171,#1172,#1173));
#324=EDGE_LOOP('',(#1174,#1175,#1176,#1177));
#325=EDGE_LOOP('',(#1178,#1179,#1180));
#326=EDGE_LOOP('',(#1181,#1182,#1183));
#327=EDGE_LOOP('',(#1184,#1185,#1186));
#328=EDGE_LOOP('',(#1187,#1188,#1189));
#329=EDGE_LOOP('',(#1190,#1191,#1192));
#330=EDGE_LOOP('',(#1193,#1194,#1195));
#331=EDGE_LOOP('',(#1196,#1197,#1198,#1199));
#332=EDGE_LOOP('',(#1200,#1201,#1202,#1203));
#333=EDGE_LOOP('',(#1204,#1205,#1206,#1207));
#334=EDGE_LOOP('',(#1208,#1209,#1210,#1211));
#335=EDGE_LOOP('',(#1212,#1213,#1214,#1215));
#336=EDGE_LOOP('',(#1216,#1217,#1218,#1219));
#337=EDGE_LOOP('',(#1220,#1221,#1222,#1223));
#338=EDGE_LOOP('',(#1224));
#339=EDGE_LOOP('',(#1225));
#433=LINE('',#2375,#552);
#434=LINE('',#2377,#553);
#435=LINE('',#2379,#554);
#436=LINE('',#2381,#555);
#437=LINE('',#2383,#556);
#438=LINE('',#2384,#557);
#439=LINE('',#2388,#558);
#440=LINE('',#2392,#559);
#441=LINE('',#2394,#560);
#442=LINE('',#2395,#561);
#443=LINE('',#2398,#562);
#444=LINE('',#2399,#563);
#445=LINE('',#2402,#564);
#446=LINE('',#2403,#565);
#447=LINE('',#2406,#566);
#448=LINE('',#2407,#567);
#449=LINE('',#2410,#568);
#450=LINE('',#2411,#569);
#451=LINE('',#2413,#570);
#452=LINE('',#2415,#571);
#453=LINE('',#2416,#572);
#454=LINE('',#2418,#573);
#455=LINE('',#2420,#574);
#456=LINE('',#2422,#575);
#457=LINE('',#2424,#576);
#458=LINE('',#2428,#577);
#552=VECTOR('',#1904,10.);
#553=VECTOR('',#1905,10.);
#554=VECTOR('',#1906,10.);
#555=VECTOR('',#1907,10.);
#556=VECTOR('',#1908,10.);
#557=VECTOR('',#1909,10.);
#558=VECTOR('',#1914,15.);
#559=VECTOR('',#1917,9.99999999999999);
#560=VECTOR('',#1918,10.);
#561=VECTOR('',#1919,10.);
#562=VECTOR('',#1922,10.);
#563=VECTOR('',#1923,10.);
#564=VECTOR('',#1926,10.);
#565=VECTOR('',#1927,9.99999999999999);
#566=VECTOR('',#1930,10.);
#567=VECTOR('',#1931,10.);
#568=VECTOR('',#1934,10.);
#569=VECTOR('',#1935,10.);
#570=VECTOR('',#1938,9.99999999999999);
#571=VECTOR('',#1941,10.);
#572=VECTOR('',#1942,10.);
#573=VECTOR('',#1945,10.);
#574=VECTOR('',#1948,10.);
#575=VECTOR('',#1951,10.);
#576=VECTOR('',#1954,10.);
#577=VECTOR('',#1959,9.89525);
#615=CIRCLE('',#1546,9.89525);
#616=CIRCLE('',#1548,15.);
#617=CIRCLE('',#1549,2.);
#618=CIRCLE('',#1550,13.);
#619=CIRCLE('',#1553,15.);
#620=CIRCLE('',#1567,9.89525);
#710=VERTEX_POINT('',#2364);
#711=VERTEX_POINT('',#2367);
#712=VERTEX_POINT('',#2369);
#713=VERTEX_POINT('',#2373);
#714=VERTEX_POINT('',#2374);
#715=VERTEX_POINT('',#2376);
#716=VERTEX_POINT('',#2378);
#717=VERTEX_POINT('',#2380);
#718=VERTEX_POINT('',#2382);
#719=VERTEX_POINT('',#2386);
#720=VERTEX_POINT('',#2390);
#721=VERTEX_POINT('',#2391);
#722=VERTEX_POINT('',#2393);
#723=VERTEX_POINT('',#2397);
#724=VERTEX_POINT('',#2401);
#725=VERTEX_POINT('',#2405);
#726=VERTEX_POINT('',#2409);
#727=VERTEX_POINT('',#2427);
#862=EDGE_CURVE('',#710,#710,#615,.T.);
#863=EDGE_CURVE('',#711,#711,#616,.T.);
#864=EDGE_CURVE('',#711,#712,#617,.T.);
#865=EDGE_CURVE('',#712,#712,#618,.T.);
#866=EDGE_CURVE('',#713,#714,#433,.T.);
#867=EDGE_CURVE('',#714,#715,#434,.T.);
#868=EDGE_CURVE('',#715,#716,#435,.T.);
#869=EDGE_CURVE('',#716,#717,#436,.T.);
#870=EDGE_CURVE('',#717,#718,#437,.T.);
#871=EDGE_CURVE('',#718,#713,#438,.T.);
#872=EDGE_CURVE('',#719,#719,#619,.T.);
#873=EDGE_CURVE('',#719,#711,#439,.T.);
#874=EDGE_CURVE('',#720,#721,#440,.T.);
#875=EDGE_CURVE('',#722,#720,#441,.T.);
#876=EDGE_CURVE('',#722,#721,#442,.T.);
#877=EDGE_CURVE('',#723,#722,#443,.T.);
#878=EDGE_CURVE('',#723,#721,#444,.T.);
#879=EDGE_CURVE('',#724,#723,#445,.T.);
#880=EDGE_CURVE('',#724,#721,#446,.T.);
#881=EDGE_CURVE('',#725,#724,#447,.T.);
#882=EDGE_CURVE('',#725,#721,#448,.T.);
#883=EDGE_CURVE('',#726,#725,#449,.T.);
#884=EDGE_CURVE('',#726,#721,#450,.T.);
#885=EDGE_CURVE('',#720,#726,#451,.T.);
#886=EDGE_CURVE('',#713,#722,#452,.T.);
#887=EDGE_CURVE('',#714,#720,#453,.T.);
#888=EDGE_CURVE('',#718,#723,#454,.T.);
#889=EDGE_CURVE('',#717,#724,#455,.T.);
#890=EDGE_CURVE('',#716,#725,#456,.T.);
#891=EDGE_CURVE('',#715,#726,#457,.T.);
#892=EDGE_CURVE('',#710,#727,#458,.T.);
#893=EDGE_CURVE('',#727,#727,#620,.F.);
#1162=ORIENTED_EDGE('',*,*,#862,.F.);
#1163=ORIENTED_EDGE('',*,*,#863,.T.);
#1164=ORIENTED_EDGE('',*,*,#864,.T.);
#1165=ORIENTED_EDGE('',*,*,#865,.T.);
#1166=ORIENTED_EDGE('',*,*,#864,.F.);
#1167=ORIENTED_EDGE('',*,*,#865,.F.);
#1168=ORIENTED_EDGE('',*,*,#866,.T.);
#1169=ORIENTED_EDGE('',*,*,#867,.T.);
#1170=ORIENTED_EDGE('',*,*,#868,.T.);
#1171=ORIENTED_EDGE('',*,*,#869,.T.);
#1172=ORIENTED_EDGE('',*,*,#870,.T.);
#1173=ORIENTED_EDGE('',*,*,#871,.T.);
#1174=ORIENTED_EDGE('',*,*,#872,.F.);
#1175=ORIENTED_EDGE('',*,*,#873,.T.);
#1176=ORIENTED_EDGE('',*,*,#863,.F.);
#1177=ORIENTED_EDGE('',*,*,#873,.F.);
#1178=ORIENTED_EDGE('',*,*,#874,.F.);
#1179=ORIENTED_EDGE('',*,*,#875,.F.);
#1180=ORIENTED_EDGE('',*,*,#876,.T.);
#1181=ORIENTED_EDGE('',*,*,#876,.F.);
#1182=ORIENTED_EDGE('',*,*,#877,.F.);
#1183=ORIENTED_EDGE('',*,*,#878,.T.);
#1184=ORIENTED_EDGE('',*,*,#878,.F.);
#1185=ORIENTED_EDGE('',*,*,#879,.F.);
#1186=ORIENTED_EDGE('',*,*,#880,.T.);
#1187=ORIENTED_EDGE('',*,*,#880,.F.);
#1188=ORIENTED_EDGE('',*,*,#881,.F.);
#1189=ORIENTED_EDGE('',*,*,#882,.T.);
#1190=ORIENTED_EDGE('',*,*,#882,.F.);
#1191=ORIENTED_EDGE('',*,*,#883,.F.);
#1192=ORIENTED_EDGE('',*,*,#884,.T.);
#1193=ORIENTED_EDGE('',*,*,#884,.F.);
#1194=ORIENTED_EDGE('',*,*,#885,.F.);
#1195=ORIENTED_EDGE('',*,*,#874,.T.);
#1196=ORIENTED_EDGE('',*,*,#866,.F.);
#1197=ORIENTED_EDGE('',*,*,#886,.T.);
#1198=ORIENTED_EDGE('',*,*,#875,.T.);
#1199=ORIENTED_EDGE('',*,*,#887,.F.);
#1200=ORIENTED_EDGE('',*,*,#871,.F.);
#1201=ORIENTED_EDGE('',*,*,#888,.T.);
#1202=ORIENTED_EDGE('',*,*,#877,.T.);
#1203=ORIENTED_EDGE('',*,*,#886,.F.);
#1204=ORIENTED_EDGE('',*,*,#870,.F.);
#1205=ORIENTED_EDGE('',*,*,#889,.T.);
#1206=ORIENTED_EDGE('',*,*,#879,.T.);
#1207=ORIENTED_EDGE('',*,*,#888,.F.);
#1208=ORIENTED_EDGE('',*,*,#869,.F.);
#1209=ORIENTED_EDGE('',*,*,#890,.T.);
#1210=ORIENTED_EDGE('',*,*,#881,.T.);
#1211=ORIENTED_EDGE('',*,*,#889,.F.);
#1212=ORIENTED_EDGE('',*,*,#868,.F.);
#1213=ORIENTED_EDGE('',*,*,#891,.T.);
#1214=ORIENTED_EDGE('',*,*,#883,.T.);
#1215=ORIENTED_EDGE('',*,*,#890,.F.);
#1216=ORIENTED_EDGE('',*,*,#867,.F.);
#1217=ORIENTED_EDGE('',*,*,#887,.T.);
#1218=ORIENTED_EDGE('',*,*,#885,.T.);
#1219=ORIENTED_EDGE('',*,*,#891,.F.);
#1220=ORIENTED_EDGE('',*,*,#862,.T.);
#1221=ORIENTED_EDGE('',*,*,#892,.T.);
#1222=ORIENTED_EDGE('',*,*,#893,.T.);
#1223=ORIENTED_EDGE('',*,*,#892,.F.);
#1224=ORIENTED_EDGE('',*,*,#872,.T.);
#1225=ORIENTED_EDGE('',*,*,#893,.F.);
#1245=CYLINDRICAL_SURFACE('',#1552,15.);
#1246=CYLINDRICAL_SURFACE('',#1566,9.89525);
#1309=ADVANCED_FACE('',(#227),#150,.T.);
#1310=ADVANCED_FACE('',(#228),#51,.T.);
#1311=ADVANCED_FACE('',(#229,#70),#151,.T.);
#1312=ADVANCED_FACE('',(#230),#1245,.T.);
#1313=ADVANCED_FACE('',(#231),#152,.F.);
#1314=ADVANCED_FACE('',(#232),#153,.F.);
#1315=ADVANCED_FACE('',(#233),#154,.F.);
#1316=ADVANCED_FACE('',(#234),#155,.F.);
#1317=ADVANCED_FACE('',(#235),#156,.F.);
#1318=ADVANCED_FACE('',(#236),#157,.F.);
#1319=ADVANCED_FACE('',(#237),#158,.F.);
#1320=ADVANCED_FACE('',(#238),#159,.F.);
#1321=ADVANCED_FACE('',(#239),#160,.F.);
#1322=ADVANCED_FACE('',(#240),#161,.F.);
#1323=ADVANCED_FACE('',(#241),#162,.F.);
#1324=ADVANCED_FACE('',(#242),#163,.F.);
#1325=ADVANCED_FACE('',(#243),#1246,.T.);
#1326=ADVANCED_FACE('',(#244,#71),#164,.T.);
#1335=CLOSED_SHELL('',(#1309,#1310,#1311,#1312,#1313,#1314,#1315,#1316,
#1317,#1318,#1319,#1320,#1321,#1322,#1323,#1324,#1325,#1326));
#1544=AXIS2_PLACEMENT_3D('',#2362,#1888,#1889);
#1545=AXIS2_PLACEMENT_3D('',#2363,#1890,#1891);
#1546=AXIS2_PLACEMENT_3D('',#2365,#1892,#1893);
#1547=AXIS2_PLACEMENT_3D('',#2366,#1894,#1895);
#1548=AXIS2_PLACEMENT_3D('',#2368,#1896,#1897);
#1549=AXIS2_PLACEMENT_3D('',#2370,#1898,#1899);
#1550=AXIS2_PLACEMENT_3D('',#2371,#1900,#1901);
#1551=AXIS2_PLACEMENT_3D('',#2372,#1902,#1903);
#1552=AXIS2_PLACEMENT_3D('',#2385,#1910,#1911);
#1553=AXIS2_PLACEMENT_3D('',#2387,#1912,#1913);
#1554=AXIS2_PLACEMENT_3D('',#2389,#1915,#1916);
#1555=AXIS2_PLACEMENT_3D('',#2396,#1920,#1921);
#1556=AXIS2_PLACEMENT_3D('',#2400,#1924,#1925);
#1557=AXIS2_PLACEMENT_3D('',#2404,#1928,#1929);
#1558=AXIS2_PLACEMENT_3D('',#2408,#1932,#1933);
#1559=AXIS2_PLACEMENT_3D('',#2412,#1936,#1937);
#1560=AXIS2_PLACEMENT_3D('',#2414,#1939,#1940);
#1561=AXIS2_PLACEMENT_3D('',#2417,#1943,#1944);
#1562=AXIS2_PLACEMENT_3D('',#2419,#1946,#1947);
#1563=AXIS2_PLACEMENT_3D('',#2421,#1949,#1950);
#1564=AXIS2_PLACEMENT_3D('',#2423,#1952,#1953);
#1565=AXIS2_PLACEMENT_3D('',#2425,#1955,#1956);
#1566=AXIS2_PLACEMENT_3D('',#2426,#1957,#1958);
#1567=AXIS2_PLACEMENT_3D('',#2429,#1960,#1961);
#1568=AXIS2_PLACEMENT_3D('',#2430,#1962,#1963);
#1888=DIRECTION('axis',(0.,0.,1.));
#1889=DIRECTION('refdir',(1.,0.,0.));
#1890=DIRECTION('center_axis',(-1.74459937578421E-17,-4.95164123815957E-15,
-1.));
#1891=DIRECTION('ref_axis',(1.,-6.93889390390722E-16,-1.74459937578387E-17));
#1892=DIRECTION('center_axis',(1.74459937578421E-17,4.95164123815957E-15,
1.));
#1893=DIRECTION('ref_axis',(-1.,0.,-2.92476088651957E-15));
#1894=DIRECTION('center_axis',(2.92476088651957E-15,0.,-1.));
#1895=DIRECTION('ref_axis',(-1.,0.,-3.0790185216271E-15));
#1896=DIRECTION('center_axis',(-2.92476088651957E-15,0.,1.));
#1897=DIRECTION('ref_axis',(1.,0.,2.92476088651957E-15));
#1898=DIRECTION('center_axis',(-1.22464679914735E-16,-1.,-3.58179905794757E-31));
#1899=DIRECTION('ref_axis',(1.,-1.22464679914735E-16,2.96059473233375E-15));
#1900=DIRECTION('center_axis',(2.92476088651957E-15,0.,-1.));
#1901=DIRECTION('ref_axis',(1.,0.,2.92476088651957E-15));
#1902=DIRECTION('center_axis',(-2.92476088651957E-15,0.,1.));
#1903=DIRECTION('ref_axis',(1.,0.,2.92476088651957E-15));
#1904=DIRECTION('',(-0.866025403784439,-0.5,-2.53291722772105E-15));
#1905=DIRECTION('',(-0.866025403784439,0.5,-2.53291722772105E-15));
#1906=DIRECTION('',(6.78692712841258E-16,1.,1.98501390048397E-30));
#1907=DIRECTION('',(0.866025403784439,0.5,2.53291722772105E-15));
#1908=DIRECTION('',(0.866025403784439,-0.5,2.53291722772105E-15));
#1909=DIRECTION('',(-1.1311545214021E-16,-1.,-3.30835650080662E-31));
#1910=DIRECTION('center_axis',(2.92476088651957E-15,0.,-1.));
#1911=DIRECTION('ref_axis',(-1.,0.,-2.92476088651957E-15));
#1912=DIRECTION('center_axis',(2.92476088651957E-15,0.,-1.));
#1913=DIRECTION('ref_axis',(1.,0.,2.92476088651957E-15));
#1914=DIRECTION('',(-2.92476088651957E-15,0.,1.));
#1915=DIRECTION('center_axis',(0.0435778713738291,-0.0754790873051733,-0.996194698091746));
#1916=DIRECTION('ref_axis',(-0.866025403784439,-0.5,-3.35810244624808E-17));
#1917=DIRECTION('',(3.18762329165829E-16,0.997141949694316,-0.0755508581011305));
#1918=DIRECTION('',(-0.866025403784439,-0.5,0.));
#1919=DIRECTION('',(-0.863550259614423,0.498570974847158,-0.0755508581011305));
#1920=DIRECTION('center_axis',(0.0871557427476581,-9.85866124751715E-18,
-0.996194698091746));
#1921=DIRECTION('ref_axis',(-1.1311545214021E-16,-1.,-2.40019600399866E-32));
#1922=DIRECTION('',(-1.1311545214021E-16,-1.,0.));
#1923=DIRECTION('',(-0.863550259614423,-0.498570974847158,-0.0755508581011305));
#1924=DIRECTION('center_axis',(0.0435778713738291,0.0754790873051733,-0.996194698091746));
#1925=DIRECTION('ref_axis',(0.866025403784439,-0.5,3.35810244624808E-17));
#1926=DIRECTION('',(0.866025403784439,-0.5,0.));
#1927=DIRECTION('',(-1.59381164582915E-16,-0.997141949694316,-0.0755508581011305));
#1928=DIRECTION('center_axis',(-0.043577871373829,0.0754790873051733,-0.996194698091746));
#1929=DIRECTION('ref_axis',(0.866025403784439,0.5,4.96857023844059E-17));
#1930=DIRECTION('',(0.866025403784439,0.5,0.));
#1931=DIRECTION('',(0.863550259614422,-0.498570974847159,-0.0755508581011305));
#1932=DIRECTION('center_axis',(-0.0871557427476581,5.91519674851029E-17,
-0.996194698091746));
#1933=DIRECTION('ref_axis',(6.78692712841258E-16,1.,4.0854062437599E-32));
#1934=DIRECTION('',(6.78692712841258E-16,1.,0.));
#1935=DIRECTION('',(0.863550259614423,0.498570974847158,-0.0755508581011305));
#1936=DIRECTION('center_axis',(-0.0435778713738291,-0.0754790873051733,
-0.996194698091746));
#1937=DIRECTION('ref_axis',(-0.866025403784439,0.5,3.35810244624808E-17));
#1938=DIRECTION('',(-0.866025403784438,0.5,0.));
#1939=DIRECTION('center_axis',(0.5,-0.866025403784439,0.));
#1940=DIRECTION('ref_axis',(-0.866025403784439,-0.5,0.));
#1941=DIRECTION('',(0.,0.,-1.));
#1942=DIRECTION('',(0.,0.,-1.));
#1943=DIRECTION('center_axis',(1.,-1.1311545214021E-16,0.));
#1944=DIRECTION('ref_axis',(-1.1311545214021E-16,-1.,0.));
#1945=DIRECTION('',(0.,0.,-1.));
#1946=DIRECTION('center_axis',(0.5,0.866025403784439,0.));
#1947=DIRECTION('ref_axis',(0.866025403784439,-0.5,0.));
#1948=DIRECTION('',(0.,0.,-1.));
#1949=DIRECTION('center_axis',(-0.5,0.866025403784439,0.));
#1950=DIRECTION('ref_axis',(0.866025403784439,0.5,0.));
#1951=DIRECTION('',(0.,0.,-1.));
#1952=DIRECTION('center_axis',(-1.,6.78692712841258E-16,0.));
#1953=DIRECTION('ref_axis',(6.78692712841258E-16,1.,0.));
#1954=DIRECTION('',(0.,0.,-1.));
#1955=DIRECTION('center_axis',(-0.5,-0.866025403784439,0.));
#1956=DIRECTION('ref_axis',(-0.866025403784439,0.5,0.));
#1957=DIRECTION('center_axis',(2.92476088651957E-15,0.,-1.));
#1958=DIRECTION('ref_axis',(-1.,0.,-2.92476088651957E-15));
#1959=DIRECTION('',(-2.92476088651957E-15,0.,1.));
#1960=DIRECTION('center_axis',(-2.92476088651957E-15,0.,1.));
#1961=DIRECTION('ref_axis',(-1.,0.,-2.92476088651957E-15));
#1962=DIRECTION('center_axis',(2.92476088651957E-15,0.,-1.));
#1963=DIRECTION('ref_axis',(-1.,0.,-2.92476088651957E-15));
#2362=CARTESIAN_POINT('',(0.,0.,0.));
#2363=CARTESIAN_POINT('Origin',(-1.4210854715202E-13,3.00426815946881E-13,
-10.0000000000003));
#2364=CARTESIAN_POINT('',(9.89524999999999,-1.21181862392628E-15,-10.0000000000004));
#2365=CARTESIAN_POINT('Origin',(-7.97007865091842E-15,0.,-10.0000000000003));
#2366=CARTESIAN_POINT('Origin',(-8.98633834734665E-14,0.,17.9999999999997));
#2367=CARTESIAN_POINT('',(14.9999999999999,-1.83697019872103E-15,17.9999999999997));
#2368=CARTESIAN_POINT('Origin',(-8.98633834734665E-14,0.,17.9999999999997));
#2369=CARTESIAN_POINT('',(12.9999999999999,-1.59204083889156E-15,19.9999999999997));
#2370=CARTESIAN_POINT('Origin',(12.9999999999999,-1.59204083889156E-15,
17.9999999999997));
#2371=CARTESIAN_POINT('Origin',(-9.57129052465056E-14,0.,19.9999999999997));
#2372=CARTESIAN_POINT('Origin',(-15.0000000000001,0.,19.9999999999996));
#2373=CARTESIAN_POINT('',(8.5,-4.90747728811182,20.));
#2374=CARTESIAN_POINT('',(3.33066907387547E-15,-9.81495457622364,20.));
#2375=CARTESIAN_POINT('',(0.749999999999985,-9.38194187433143,19.9999999999997));
#2376=CARTESIAN_POINT('',(-8.50000000000001,-4.90747728811181,20.));
#2377=CARTESIAN_POINT('',(-7.75000000000002,-5.34048999000403,19.9999999999997));
#2378=CARTESIAN_POINT('',(-8.5,4.90747728811182,20.));
#2379=CARTESIAN_POINT('',(-8.50000000000001,-2.45373864405591,19.9999999999997));
#2380=CARTESIAN_POINT('',(1.12757025938492E-15,9.81495457622364,20.));
#2381=CARTESIAN_POINT('',(-12.,2.88675134594812,19.9999999999997));
#2382=CARTESIAN_POINT('',(8.5,4.90747728811182,20.));
#2383=CARTESIAN_POINT('',(-3.50000000000002,11.8356805183873,19.9999999999997));
#2384=CARTESIAN_POINT('',(8.5,2.45373864405591,19.9999999999997));
#2385=CARTESIAN_POINT('Origin',(-6.64652963813099E-14,0.,9.99999999999969));
#2386=CARTESIAN_POINT('',(14.9999999999999,-1.83697019872103E-15,-2.67563748934663E-13));
#2387=CARTESIAN_POINT('Origin',(-3.72176875161141E-14,0.,-3.1184928405981E-13));
#2388=CARTESIAN_POINT('',(14.9999999999999,-1.83697019872103E-15,9.99999999999973));
#2389=CARTESIAN_POINT('Origin',(3.33066907387547E-15,-9.81495457622364,
10.));
#2390=CARTESIAN_POINT('',(3.33066907387547E-15,-9.81495457622364,10.));
#2391=CARTESIAN_POINT('',(-9.72987853259607E-16,-2.22044604925031E-15,9.25634636002965));
#2392=CARTESIAN_POINT('',(-3.33066907387547E-15,-7.37522170588592,9.81514777113925));
#2393=CARTESIAN_POINT('',(8.5,-4.90747728811182,10.));
#2394=CARTESIAN_POINT('',(3.19337359890869E-15,-9.81495457622364,10.));
#2395=CARTESIAN_POINT('',(6.38712935583962,-3.68761085294296,9.81514777113925));
#2396=CARTESIAN_POINT('Origin',(8.5,-4.90747728811182,10.));
#2397=CARTESIAN_POINT('',(8.5,4.90747728811182,10.));
#2398=CARTESIAN_POINT('',(8.5,-4.90747728811182,10.));
#2399=CARTESIAN_POINT('',(6.38712935583961,3.68761085294296,9.81514777113925));
#2400=CARTESIAN_POINT('Origin',(8.5,4.90747728811182,10.));
#2401=CARTESIAN_POINT('',(1.11022302462516E-15,9.81495457622364,10.));
#2402=CARTESIAN_POINT('',(8.5,4.90747728811182,10.));
#2403=CARTESIAN_POINT('',(-2.22044604925031E-15,7.37522170588592,9.81514777113925));
#2404=CARTESIAN_POINT('Origin',(1.11022302462516E-15,9.81495457622364,10.));
#2405=CARTESIAN_POINT('',(-8.5,4.90747728811182,10.));
#2406=CARTESIAN_POINT('',(1.12757025938492E-15,9.81495457622364,10.));
#2407=CARTESIAN_POINT('',(-6.38712935583961,3.68761085294296,9.81514777113925));
#2408=CARTESIAN_POINT('Origin',(-8.5,4.90747728811182,10.));
#2409=CARTESIAN_POINT('',(-8.50000000000001,-4.90747728811181,10.));
#2410=CARTESIAN_POINT('',(-8.5,4.90747728811182,10.));
#2411=CARTESIAN_POINT('',(-6.38712935583962,-3.68761085294295,9.81514777113925));
#2412=CARTESIAN_POINT('Origin',(-8.50000000000001,-4.90747728811181,10.));
#2413=CARTESIAN_POINT('',(-8.50000000000001,-4.90747728811181,10.));
#2414=CARTESIAN_POINT('Origin',(8.5,-4.90747728811182,20.));
#2415=CARTESIAN_POINT('',(8.5,-4.90747728811182,20.));
#2416=CARTESIAN_POINT('',(3.33066907387547E-15,-9.81495457622364,20.));
#2417=CARTESIAN_POINT('Origin',(8.5,4.90747728811182,20.));
#2418=CARTESIAN_POINT('',(8.5,4.90747728811182,20.));
#2419=CARTESIAN_POINT('Origin',(1.11022302462516E-15,9.81495457622364,20.));
#2420=CARTESIAN_POINT('',(1.12757025938492E-15,9.81495457622364,20.));
#2421=CARTESIAN_POINT('Origin',(-8.5,4.90747728811182,20.));
#2422=CARTESIAN_POINT('',(-8.5,4.90747728811182,20.));
#2423=CARTESIAN_POINT('Origin',(-8.50000000000001,-4.90747728811181,20.));
#2424=CARTESIAN_POINT('',(-8.50000000000001,-4.90747728811181,20.));
#2425=CARTESIAN_POINT('Origin',(3.33066907387547E-15,-9.81495457622364,
20.));
#2426=CARTESIAN_POINT('Origin',(-7.9700786509191E-15,0.,-10.0000000000001));
#2427=CARTESIAN_POINT('',(9.89524999999996,1.21181862392628E-15,-1.32099810487998E-13));
#2428=CARTESIAN_POINT('',(9.89524999999999,-1.21181862392628E-15,-10.0000000000001));
#2429=CARTESIAN_POINT('Origin',(-3.72176875161146E-14,0.,-1.60982338570648E-13));
#2430=CARTESIAN_POINT('Origin',(-10.,0.,-1.89717705257387E-13));
#2450=UNCERTAINTY_MEASURE_WITH_UNIT(LENGTH_MEASURE(0.01),#2463,
'DISTANCE_ACCURACY_VALUE',
'Maximum model space distance between geometric entities at asserted c
onnectivities');
#2451=UNCERTAINTY_MEASURE_WITH_UNIT(LENGTH_MEASURE(0.01),#2463,
'DISTANCE_ACCURACY_VALUE',
'Maximum model space distance between geometric entities at asserted c
onnectivities');
#2461=(
GEOMETRIC_REPRESENTATION_CONTEXT(3)
GLOBAL_UNCERTAINTY_ASSIGNED_CONTEXT((#2450))
GLOBAL_UNIT_ASSIGNED_CONTEXT((#2463,#2465,#2466))
REPRESENTATION_CONTEXT('','3D')
);
#2462=(
GEOMETRIC_REPRESENTATION_CONTEXT(3)
GLOBAL_UNCERTAINTY_ASSIGNED_CONTEXT((#2451))
GLOBAL_UNIT_ASSIGNED_CONTEXT((#2463,#2465,#2466))
REPRESENTATION_CONTEXT('','3D')
);
#2463=(
LENGTH_UNIT()
NAMED_UNIT(*)
SI_UNIT(.MILLI.,.METRE.)
);
#2465=(
NAMED_UNIT(*)
PLANE_ANGLE_UNIT()
SI_UNIT($,.RADIAN.)
);
#2466=(
NAMED_UNIT(*)
SI_UNIT($,.STERADIAN.)
SOLID_ANGLE_UNIT()
);
#2476=SHAPE_DEFINITION_REPRESENTATION(#2486,#2506);
#2486=PRODUCT_DEFINITION_SHAPE('',$,#2517);
#2506=SHAPE_REPRESENTATION('',(#1544),#2461);
#2507=PRODUCT_DEFINITION_CONTEXT('part definition',#2539,'design');
#2517=PRODUCT_DEFINITION(
'BSHCS ASME B18.3.1M - M20x2.5 x 20 Steel Grade 2 Plain_1','Screw_02',#2527,
#2507);
#2527=PRODUCT_DEFINITION_FORMATION('',$,#2550);
#2539=APPLICATION_CONTEXT(
'Core Data for Automotive Mechanical Design Process');
#2540=PRODUCT_CONTEXT('part definition',#2539,'mechanical');
#2550=PRODUCT(
'BSHCS ASME B18.3.1M - M20x2.5 x 20 Steel Grade 2 Plain_1','Screw_02',
'Broached Hexagon Socket Head Cap Screw ASME B18.3.1M - M20x2.5 x 20',(#2540));
#2552=PRESENTATION_STYLE_ASSIGNMENT((#2555));
#2555=SURFACE_STYLE_USAGE(.BOTH.,#2558);
#2558=SURFACE_SIDE_STYLE('',(#2561));
#2561=SURFACE_STYLE_FILL_AREA(#2564);
#2564=FILL_AREA_STYLE('Opaque(160,160,160)',(#2567));
#2567=FILL_AREA_STYLE_COLOUR('Opaque(160,160,160)',#2570);
#2570=COLOUR_RGB('Opaque(160,160,160)', 0.09019608, 0.27058824, 0.51372549);
ENDSEC;
END-ISO-10303-21;
